ISO-10303-21;
HEADER;
/* Generated by software containing ST-Developer
 * from STEP Tools, Inc. (www.steptools.com) 
 */

FILE_DESCRIPTION(
/* description */ ('XY cross-slide table'),
/* implementation_level */ '2;1');

FILE_NAME(
/* name */ 'Y Stage - 07 Nut bracket.step',
/* time_stamp */ '2026-10-28T03:22:46-07:00',
/* author */ (''),
/* organization */ (''),
/* preprocessor_version */ 'ST-DEVELOPER v20.2',
/* originating_system */ 'Autodesk Translation Framework v15.17.0.0',
/* authorisation */ '');

FILE_SCHEMA (('AUTOMOTIVE_DESIGN { 1 0 10303 214 3 1 1 }'));
ENDSEC;

DATA;
#10=MECHANICAL_DESIGN_GEOMETRIC_PRESENTATION_REPRESENTATION('',(#1764),#62984);
#1568=SHAPE_REPRESENTATION_RELATIONSHIP('SRR','None',#63426,#1651);
#1651=ADVANCED_BREP_SHAPE_REPRESENTATION('',(#1872),#62963);
#1764=STYLED_ITEM('',(#63919),#1872);
#1872=MANIFOLD_SOLID_BREP('Body1',#23063);
#2244=FACE_BOUND('',#5502,.T.);
#2245=FACE_BOUND('',#5503,.T.);
#2246=FACE_BOUND('',#5504,.T.);
#2247=FACE_BOUND('',#5505,.T.);
#2248=FACE_BOUND('',#5508,.T.);
#2249=FACE_BOUND('',#5510,.T.);
#2250=FACE_BOUND('',#5511,.T.);
#2251=FACE_BOUND('',#5512,.T.);
#2252=FACE_BOUND('',#5513,.T.);
#2718=PLANE('',#25871);
#2719=PLANE('',#25875);
#2720=PLANE('',#25879);
#2721=PLANE('',#25883);
#2722=PLANE('',#25887);
#2723=PLANE('',#25891);
#2724=PLANE('',#25895);
#2725=PLANE('',#25899);
#2726=PLANE('',#25900);
#2727=PLANE('',#25901);
#2728=PLANE('',#25902);
#2729=PLANE('',#25903);
#2730=PLANE('',#25904);
#3814=FACE_OUTER_BOUND('',#5485,.T.);
#3815=FACE_OUTER_BOUND('',#5486,.T.);
#3816=FACE_OUTER_BOUND('',#5487,.T.);
#3817=FACE_OUTER_BOUND('',#5488,.T.);
#3818=FACE_OUTER_BOUND('',#5489,.T.);
#3819=FACE_OUTER_BOUND('',#5490,.T.);
#3820=FACE_OUTER_BOUND('',#5491,.T.);
#3821=FACE_OUTER_BOUND('',#5492,.T.);
#3822=FACE_OUTER_BOUND('',#5493,.T.);
#3823=FACE_OUTER_BOUND('',#5494,.T.);
#3824=FACE_OUTER_BOUND('',#5495,.T.);
#3825=FACE_OUTER_BOUND('',#5496,.T.);
#3826=FACE_OUTER_BOUND('',#5497,.T.);
#3827=FACE_OUTER_BOUND('',#5498,.T.);
#3828=FACE_OUTER_BOUND('',#5499,.T.);
#3829=FACE_OUTER_BOUND('',#5500,.T.);
#3830=FACE_OUTER_BOUND('',#5501,.T.);
#3831=FACE_OUTER_BOUND('',#5506,.T.);
#3832=FACE_OUTER_BOUND('',#5507,.T.);
#3833=FACE_OUTER_BOUND('',#5509,.T.);
#3834=FACE_OUTER_BOUND('',#5514,.T.);
#5485=EDGE_LOOP('',(#19218,#19219,#19220,#19221));
#5486=EDGE_LOOP('',(#19222));
#5487=EDGE_LOOP('',(#19223,#19224,#19225,#19226));
#5488=EDGE_LOOP('',(#19227));
#5489=EDGE_LOOP('',(#19228,#19229,#19230,#19231));
#5490=EDGE_LOOP('',(#19232));
#5491=EDGE_LOOP('',(#19233,#19234,#19235,#19236));
#5492=EDGE_LOOP('',(#19237));
#5493=EDGE_LOOP('',(#19238,#19239,#19240,#19241));
#5494=EDGE_LOOP('',(#19242));
#5495=EDGE_LOOP('',(#19243,#19244,#19245,#19246));
#5496=EDGE_LOOP('',(#19247));
#5497=EDGE_LOOP('',(#19248,#19249,#19250,#19251));
#5498=EDGE_LOOP('',(#19252));
#5499=EDGE_LOOP('',(#19253,#19254,#19255,#19256));
#5500=EDGE_LOOP('',(#19257,#19258,#19259,#19260));
#5501=EDGE_LOOP('',(#19261,#19262,#19263,#19264));
#5502=EDGE_LOOP('',(#19265));
#5503=EDGE_LOOP('',(#19266));
#5504=EDGE_LOOP('',(#19267));
#5505=EDGE_LOOP('',(#19268));
#5506=EDGE_LOOP('',(#19269,#19270,#19271,#19272));
#5507=EDGE_LOOP('',(#19273,#19274,#19275,#19276));
#5508=EDGE_LOOP('',(#19277));
#5509=EDGE_LOOP('',(#19278,#19279,#19280,#19281));
#5510=EDGE_LOOP('',(#19282));
#5511=EDGE_LOOP('',(#19283));
#5512=EDGE_LOOP('',(#19284));
#5513=EDGE_LOOP('',(#19285));
#5514=EDGE_LOOP('',(#19286,#19287,#19288,#19289));
#6928=LINE('',#49842,#8415);
#6929=LINE('',#49849,#8416);
#6930=LINE('',#49856,#8417);
#6931=LINE('',#49863,#8418);
#6932=LINE('',#49870,#8419);
#6933=LINE('',#49877,#8420);
#6934=LINE('',#49884,#8421);
#6935=LINE('',#49891,#8422);
#6936=LINE('',#49896,#8423);
#6937=LINE('',#49898,#8424);
#6938=LINE('',#49900,#8425);
#6939=LINE('',#49901,#8426);
#6940=LINE('',#49904,#8427);
#6941=LINE('',#49906,#8428);
#6942=LINE('',#49907,#8429);
#6943=LINE('',#49910,#8430);
#6944=LINE('',#49912,#8431);
#6945=LINE('',#49913,#8432);
#6946=LINE('',#49915,#8433);
#6947=LINE('',#49916,#8434);
#8415=VECTOR('',#31223,0.210000000000001);
#8416=VECTOR('',#31232,0.210000000000001);
#8417=VECTOR('',#31241,0.210000000000001);
#8418=VECTOR('',#31250,0.210000000000001);
#8419=VECTOR('',#31259,0.165);
#8420=VECTOR('',#31268,0.165);
#8421=VECTOR('',#31277,0.165);
#8422=VECTOR('',#31286,1.11);
#8423=VECTOR('',#31291,1.);
#8424=VECTOR('',#31292,1.);
#8425=VECTOR('',#31293,1.);
#8426=VECTOR('',#31294,1.);
#8427=VECTOR('',#31297,1.);
#8428=VECTOR('',#31298,1.);
#8429=VECTOR('',#31299,1.);
#8430=VECTOR('',#31302,1.);
#8431=VECTOR('',#31303,1.);
#8432=VECTOR('',#31304,1.);
#8433=VECTOR('',#31307,1.);
#8434=VECTOR('',#31308,1.);
#9639=CIRCLE('',#25869,0.210000000000001);
#9640=CIRCLE('',#25870,0.210000000000001);
#9641=CIRCLE('',#25873,0.210000000000001);
#9642=CIRCLE('',#25874,0.210000000000001);
#9643=CIRCLE('',#25877,0.210000000000001);
#9644=CIRCLE('',#25878,0.210000000000001);
#9645=CIRCLE('',#25881,0.210000000000001);
#9646=CIRCLE('',#25882,0.210000000000001);
#9647=CIRCLE('',#25885,0.165);
#9648=CIRCLE('',#25886,0.165);
#9649=CIRCLE('',#25889,0.165);
#9650=CIRCLE('',#25890,0.165);
#9651=CIRCLE('',#25893,0.165);
#9652=CIRCLE('',#25894,0.165);
#9653=CIRCLE('',#25897,1.11);
#9654=CIRCLE('',#25898,1.11);
#11234=VERTEX_POINT('',#49839);
#11235=VERTEX_POINT('',#49841);
#11236=VERTEX_POINT('',#49846);
#11237=VERTEX_POINT('',#49848);
#11238=VERTEX_POINT('',#49853);
#11239=VERTEX_POINT('',#49855);
#11240=VERTEX_POINT('',#49860);
#11241=VERTEX_POINT('',#49862);
#11242=VERTEX_POINT('',#49867);
#11243=VERTEX_POINT('',#49869);
#11244=VERTEX_POINT('',#49874);
#11245=VERTEX_POINT('',#49876);
#11246=VERTEX_POINT('',#49881);
#11247=VERTEX_POINT('',#49883);
#11248=VERTEX_POINT('',#49888);
#11249=VERTEX_POINT('',#49890);
#11250=VERTEX_POINT('',#49894);
#11251=VERTEX_POINT('',#49895);
#11252=VERTEX_POINT('',#49897);
#11253=VERTEX_POINT('',#49899);
#11254=VERTEX_POINT('',#49903);
#11255=VERTEX_POINT('',#49905);
#11256=VERTEX_POINT('',#49909);
#11257=VERTEX_POINT('',#49911);
#13993=EDGE_CURVE('',#11234,#11234,#9639,.T.);
#13994=EDGE_CURVE('',#11234,#11235,#6928,.T.);
#13995=EDGE_CURVE('',#11235,#11235,#9640,.T.);
#13996=EDGE_CURVE('',#11236,#11236,#9641,.T.);
#13997=EDGE_CURVE('',#11236,#11237,#6929,.T.);
#13998=EDGE_CURVE('',#11237,#11237,#9642,.T.);
#13999=EDGE_CURVE('',#11238,#11238,#9643,.T.);
#14000=EDGE_CURVE('',#11238,#11239,#6930,.T.);
#14001=EDGE_CURVE('',#11239,#11239,#9644,.T.);
#14002=EDGE_CURVE('',#11240,#11240,#9645,.T.);
#14003=EDGE_CURVE('',#11240,#11241,#6931,.T.);
#14004=EDGE_CURVE('',#11241,#11241,#9646,.T.);
#14005=EDGE_CURVE('',#11242,#11242,#9647,.T.);
#14006=EDGE_CURVE('',#11242,#11243,#6932,.T.);
#14007=EDGE_CURVE('',#11243,#11243,#9648,.T.);
#14008=EDGE_CURVE('',#11244,#11244,#9649,.T.);
#14009=EDGE_CURVE('',#11244,#11245,#6933,.T.);
#14010=EDGE_CURVE('',#11245,#11245,#9650,.T.);
#14011=EDGE_CURVE('',#11246,#11246,#9651,.T.);
#14012=EDGE_CURVE('',#11246,#11247,#6934,.T.);
#14013=EDGE_CURVE('',#11247,#11247,#9652,.T.);
#14014=EDGE_CURVE('',#11248,#11248,#9653,.T.);
#14015=EDGE_CURVE('',#11248,#11249,#6935,.T.);
#14016=EDGE_CURVE('',#11249,#11249,#9654,.T.);
#14017=EDGE_CURVE('',#11250,#11251,#6936,.T.);
#14018=EDGE_CURVE('',#11251,#11252,#6937,.T.);
#14019=EDGE_CURVE('',#11253,#11252,#6938,.T.);
#14020=EDGE_CURVE('',#11250,#11253,#6939,.T.);
#14021=EDGE_CURVE('',#11254,#11250,#6940,.T.);
#14022=EDGE_CURVE('',#11255,#11253,#6941,.T.);
#14023=EDGE_CURVE('',#11254,#11255,#6942,.T.);
#14024=EDGE_CURVE('',#11256,#11254,#6943,.T.);
#14025=EDGE_CURVE('',#11257,#11255,#6944,.T.);
#14026=EDGE_CURVE('',#11256,#11257,#6945,.T.);
#14027=EDGE_CURVE('',#11251,#11256,#6946,.T.);
#14028=EDGE_CURVE('',#11252,#11257,#6947,.T.);
#19218=ORIENTED_EDGE('',*,*,#13993,.F.);
#19219=ORIENTED_EDGE('',*,*,#13994,.T.);
#19220=ORIENTED_EDGE('',*,*,#13995,.F.);
#19221=ORIENTED_EDGE('',*,*,#13994,.F.);
#19222=ORIENTED_EDGE('',*,*,#13993,.T.);
#19223=ORIENTED_EDGE('',*,*,#13996,.F.);
#19224=ORIENTED_EDGE('',*,*,#13997,.T.);
#19225=ORIENTED_EDGE('',*,*,#13998,.F.);
#19226=ORIENTED_EDGE('',*,*,#13997,.F.);
#19227=ORIENTED_EDGE('',*,*,#13996,.T.);
#19228=ORIENTED_EDGE('',*,*,#13999,.F.);
#19229=ORIENTED_EDGE('',*,*,#14000,.T.);
#19230=ORIENTED_EDGE('',*,*,#14001,.F.);
#19231=ORIENTED_EDGE('',*,*,#14000,.F.);
#19232=ORIENTED_EDGE('',*,*,#13999,.T.);
#19233=ORIENTED_EDGE('',*,*,#14002,.F.);
#19234=ORIENTED_EDGE('',*,*,#14003,.T.);
#19235=ORIENTED_EDGE('',*,*,#14004,.F.);
#19236=ORIENTED_EDGE('',*,*,#14003,.F.);
#19237=ORIENTED_EDGE('',*,*,#14002,.T.);
#19238=ORIENTED_EDGE('',*,*,#14005,.F.);
#19239=ORIENTED_EDGE('',*,*,#14006,.T.);
#19240=ORIENTED_EDGE('',*,*,#14007,.F.);
#19241=ORIENTED_EDGE('',*,*,#14006,.F.);
#19242=ORIENTED_EDGE('',*,*,#14005,.T.);
#19243=ORIENTED_EDGE('',*,*,#14008,.F.);
#19244=ORIENTED_EDGE('',*,*,#14009,.T.);
#19245=ORIENTED_EDGE('',*,*,#14010,.F.);
#19246=ORIENTED_EDGE('',*,*,#14009,.F.);
#19247=ORIENTED_EDGE('',*,*,#14008,.T.);
#19248=ORIENTED_EDGE('',*,*,#14011,.F.);
#19249=ORIENTED_EDGE('',*,*,#14012,.T.);
#19250=ORIENTED_EDGE('',*,*,#14013,.F.);
#19251=ORIENTED_EDGE('',*,*,#14012,.F.);
#19252=ORIENTED_EDGE('',*,*,#14011,.T.);
#19253=ORIENTED_EDGE('',*,*,#14014,.F.);
#19254=ORIENTED_EDGE('',*,*,#14015,.T.);
#19255=ORIENTED_EDGE('',*,*,#14016,.F.);
#19256=ORIENTED_EDGE('',*,*,#14015,.F.);
#19257=ORIENTED_EDGE('',*,*,#14017,.T.);
#19258=ORIENTED_EDGE('',*,*,#14018,.T.);
#19259=ORIENTED_EDGE('',*,*,#14019,.F.);
#19260=ORIENTED_EDGE('',*,*,#14020,.F.);
#19261=ORIENTED_EDGE('',*,*,#14021,.T.);
#19262=ORIENTED_EDGE('',*,*,#14020,.T.);
#19263=ORIENTED_EDGE('',*,*,#14022,.F.);
#19264=ORIENTED_EDGE('',*,*,#14023,.F.);
#19265=ORIENTED_EDGE('',*,*,#14007,.T.);
#19266=ORIENTED_EDGE('',*,*,#14010,.T.);
#19267=ORIENTED_EDGE('',*,*,#14013,.T.);
#19268=ORIENTED_EDGE('',*,*,#14016,.T.);
#19269=ORIENTED_EDGE('',*,*,#14024,.T.);
#19270=ORIENTED_EDGE('',*,*,#14023,.T.);
#19271=ORIENTED_EDGE('',*,*,#14025,.F.);
#19272=ORIENTED_EDGE('',*,*,#14026,.F.);
#19273=ORIENTED_EDGE('',*,*,#14027,.T.);
#19274=ORIENTED_EDGE('',*,*,#14026,.T.);
#19275=ORIENTED_EDGE('',*,*,#14028,.F.);
#19276=ORIENTED_EDGE('',*,*,#14018,.F.);
#19277=ORIENTED_EDGE('',*,*,#14014,.T.);
#19278=ORIENTED_EDGE('',*,*,#14028,.T.);
#19279=ORIENTED_EDGE('',*,*,#14025,.T.);
#19280=ORIENTED_EDGE('',*,*,#14022,.T.);
#19281=ORIENTED_EDGE('',*,*,#14019,.T.);
#19282=ORIENTED_EDGE('',*,*,#13995,.T.);
#19283=ORIENTED_EDGE('',*,*,#13998,.T.);
#19284=ORIENTED_EDGE('',*,*,#14001,.T.);
#19285=ORIENTED_EDGE('',*,*,#14004,.T.);
#19286=ORIENTED_EDGE('',*,*,#14027,.F.);
#19287=ORIENTED_EDGE('',*,*,#14017,.F.);
#19288=ORIENTED_EDGE('',*,*,#14021,.F.);
#19289=ORIENTED_EDGE('',*,*,#14024,.F.);
#21454=CYLINDRICAL_SURFACE('',#25868,0.210000000000001);
#21455=CYLINDRICAL_SURFACE('',#25872,0.210000000000001);
#21456=CYLINDRICAL_SURFACE('',#25876,0.210000000000001);
#21457=CYLINDRICAL_SURFACE('',#25880,0.210000000000001);
#21458=CYLINDRICAL_SURFACE('',#25884,0.165);
#21459=CYLINDRICAL_SURFACE('',#25888,0.165);
#21460=CYLINDRICAL_SURFACE('',#25892,0.165);
#21461=CYLINDRICAL_SURFACE('',#25896,1.11);
#22595=ADVANCED_FACE('',(#3814),#21454,.F.);
#22596=ADVANCED_FACE('',(#3815),#2718,.T.);
#22597=ADVANCED_FACE('',(#3816),#21455,.F.);
#22598=ADVANCED_FACE('',(#3817),#2719,.T.);
#22599=ADVANCED_FACE('',(#3818),#21456,.F.);
#22600=ADVANCED_FACE('',(#3819),#2720,.T.);
#22601=ADVANCED_FACE('',(#3820),#21457,.F.);
#22602=ADVANCED_FACE('',(#3821),#2721,.T.);
#22603=ADVANCED_FACE('',(#3822),#21458,.F.);
#22604=ADVANCED_FACE('',(#3823),#2722,.T.);
#22605=ADVANCED_FACE('',(#3824),#21459,.F.);
#22606=ADVANCED_FACE('',(#3825),#2723,.T.);
#22607=ADVANCED_FACE('',(#3826),#21460,.F.);
#22608=ADVANCED_FACE('',(#3827),#2724,.T.);
#22609=ADVANCED_FACE('',(#3828),#21461,.F.);
#22610=ADVANCED_FACE('',(#3829),#2725,.T.);
#22611=ADVANCED_FACE('',(#3830,#2244,#2245,#2246,#2247),#2726,.T.);
#22612=ADVANCED_FACE('',(#3831),#2727,.T.);
#22613=ADVANCED_FACE('',(#3832,#2248),#2728,.T.);
#22614=ADVANCED_FACE('',(#3833,#2249,#2250,#2251,#2252),#2729,.T.);
#22615=ADVANCED_FACE('',(#3834),#2730,.F.);
#23063=CLOSED_SHELL('',(#22595,#22596,#22597,#22598,#22599,#22600,#22601,
#22602,#22603,#22604,#22605,#22606,#22607,#22608,#22609,#22610,#22611,#22612,
#22613,#22614,#22615));
#25867=AXIS2_PLACEMENT_3D('',#49837,#31217,#31218);
#25868=AXIS2_PLACEMENT_3D('',#49838,#31219,#31220);
#25869=AXIS2_PLACEMENT_3D('',#49840,#31221,#31222);
#25870=AXIS2_PLACEMENT_3D('',#49843,#31224,#31225);
#25871=AXIS2_PLACEMENT_3D('',#49844,#31226,#31227);
#25872=AXIS2_PLACEMENT_3D('',#49845,#31228,#31229);
#25873=AXIS2_PLACEMENT_3D('',#49847,#31230,#31231);
#25874=AXIS2_PLACEMENT_3D('',#49850,#31233,#31234);
#25875=AXIS2_PLACEMENT_3D('',#49851,#31235,#31236);
#25876=AXIS2_PLACEMENT_3D('',#49852,#31237,#31238);
#25877=AXIS2_PLACEMENT_3D('',#49854,#31239,#31240);
#25878=AXIS2_PLACEMENT_3D('',#49857,#31242,#31243);
#25879=AXIS2_PLACEMENT_3D('',#49858,#31244,#31245);
#25880=AXIS2_PLACEMENT_3D('',#49859,#31246,#31247);
#25881=AXIS2_PLACEMENT_3D('',#49861,#31248,#31249);
#25882=AXIS2_PLACEMENT_3D('',#49864,#31251,#31252);
#25883=AXIS2_PLACEMENT_3D('',#49865,#31253,#31254);
#25884=AXIS2_PLACEMENT_3D('',#49866,#31255,#31256);
#25885=AXIS2_PLACEMENT_3D('',#49868,#31257,#31258);
#25886=AXIS2_PLACEMENT_3D('',#49871,#31260,#31261);
#25887=AXIS2_PLACEMENT_3D('',#49872,#31262,#31263);
#25888=AXIS2_PLACEMENT_3D('',#49873,#31264,#31265);
#25889=AXIS2_PLACEMENT_3D('',#49875,#31266,#31267);
#25890=AXIS2_PLACEMENT_3D('',#49878,#31269,#31270);
#25891=AXIS2_PLACEMENT_3D('',#49879,#31271,#31272);
#25892=AXIS2_PLACEMENT_3D('',#49880,#31273,#31274);
#25893=AXIS2_PLACEMENT_3D('',#49882,#31275,#31276);
#25894=AXIS2_PLACEMENT_3D('',#49885,#31278,#31279);
#25895=AXIS2_PLACEMENT_3D('',#49886,#31280,#31281);
#25896=AXIS2_PLACEMENT_3D('',#49887,#31282,#31283);
#25897=AXIS2_PLACEMENT_3D('',#49889,#31284,#31285);
#25898=AXIS2_PLACEMENT_3D('',#49892,#31287,#31288);
#25899=AXIS2_PLACEMENT_3D('',#49893,#31289,#31290);
#25900=AXIS2_PLACEMENT_3D('',#49902,#31295,#31296);
#25901=AXIS2_PLACEMENT_3D('',#49908,#31300,#31301);
#25902=AXIS2_PLACEMENT_3D('',#49914,#31305,#31306);
#25903=AXIS2_PLACEMENT_3D('',#49917,#31309,#31310);
#25904=AXIS2_PLACEMENT_3D('',#49918,#31311,#31312);
#31217=DIRECTION('axis',(0.,0.,1.));
#31218=DIRECTION('refdir',(1.,0.,0.));
#31219=DIRECTION('center_axis',(0.,0.,1.));
#31220=DIRECTION('ref_axis',(1.,0.,0.));
#31221=DIRECTION('center_axis',(0.,0.,1.));
#31222=DIRECTION('ref_axis',(1.,0.,0.));
#31223=DIRECTION('',(0.,0.,1.));
#31224=DIRECTION('center_axis',(0.,0.,-1.));
#31225=DIRECTION('ref_axis',(1.,0.,0.));
#31226=DIRECTION('center_axis',(0.,0.,1.));
#31227=DIRECTION('ref_axis',(1.,0.,0.));
#31228=DIRECTION('center_axis',(0.,0.,1.));
#31229=DIRECTION('ref_axis',(1.,0.,0.));
#31230=DIRECTION('center_axis',(0.,0.,1.));
#31231=DIRECTION('ref_axis',(1.,0.,0.));
#31232=DIRECTION('',(0.,0.,1.));
#31233=DIRECTION('center_axis',(0.,0.,-1.));
#31234=DIRECTION('ref_axis',(1.,0.,0.));
#31235=DIRECTION('center_axis',(0.,0.,1.));
#31236=DIRECTION('ref_axis',(1.,0.,0.));
#31237=DIRECTION('center_axis',(0.,0.,1.));
#31238=DIRECTION('ref_axis',(1.,0.,0.));
#31239=DIRECTION('center_axis',(0.,0.,1.));
#31240=DIRECTION('ref_axis',(1.,0.,0.));
#31241=DIRECTION('',(0.,0.,1.));
#31242=DIRECTION('center_axis',(0.,0.,-1.));
#31243=DIRECTION('ref_axis',(1.,0.,0.));
#31244=DIRECTION('center_axis',(0.,0.,1.));
#31245=DIRECTION('ref_axis',(1.,0.,0.));
#31246=DIRECTION('center_axis',(0.,0.,1.));
#31247=DIRECTION('ref_axis',(1.,0.,0.));
#31248=DIRECTION('center_axis',(0.,0.,1.));
#31249=DIRECTION('ref_axis',(1.,0.,0.));
#31250=DIRECTION('',(0.,0.,1.));
#31251=DIRECTION('center_axis',(0.,0.,-1.));
#31252=DIRECTION('ref_axis',(1.,0.,0.));
#31253=DIRECTION('center_axis',(0.,0.,1.));
#31254=DIRECTION('ref_axis',(1.,0.,0.));
#31255=DIRECTION('center_axis',(1.,0.,0.));
#31256=DIRECTION('ref_axis',(0.,0.,-1.));
#31257=DIRECTION('center_axis',(1.,0.,0.));
#31258=DIRECTION('ref_axis',(0.,0.,-1.));
#31259=DIRECTION('',(1.,0.,0.));
#31260=DIRECTION('center_axis',(-1.,0.,0.));
#31261=DIRECTION('ref_axis',(0.,0.,-1.));
#31262=DIRECTION('center_axis',(1.,0.,0.));
#31263=DIRECTION('ref_axis',(0.,0.,-1.));
#31264=DIRECTION('center_axis',(1.,0.,0.));
#31265=DIRECTION('ref_axis',(0.,0.,-1.));
#31266=DIRECTION('center_axis',(1.,0.,0.));
#31267=DIRECTION('ref_axis',(0.,0.,-1.));
#31268=DIRECTION('',(1.,0.,0.));
#31269=DIRECTION('center_axis',(-1.,0.,0.));
#31270=DIRECTION('ref_axis',(0.,0.,-1.));
#31271=DIRECTION('center_axis',(1.,0.,0.));
#31272=DIRECTION('ref_axis',(0.,0.,-1.));
#31273=DIRECTION('center_axis',(1.,0.,0.));
#31274=DIRECTION('ref_axis',(0.,0.,-1.));
#31275=DIRECTION('center_axis',(1.,0.,0.));
#31276=DIRECTION('ref_axis',(0.,0.,-1.));
#31277=DIRECTION('',(1.,0.,0.));
#31278=DIRECTION('center_axis',(-1.,0.,0.));
#31279=DIRECTION('ref_axis',(0.,0.,-1.));
#31280=DIRECTION('center_axis',(1.,0.,0.));
#31281=DIRECTION('ref_axis',(0.,0.,-1.));
#31282=DIRECTION('center_axis',(1.,0.,0.));
#31283=DIRECTION('ref_axis',(0.,0.,-1.));
#31284=DIRECTION('center_axis',(1.,0.,0.));
#31285=DIRECTION('ref_axis',(0.,0.,-1.));
#31286=DIRECTION('',(1.,0.,0.));
#31287=DIRECTION('center_axis',(-1.,0.,0.));
#31288=DIRECTION('ref_axis',(0.,0.,-1.));
#31289=DIRECTION('center_axis',(0.,1.,0.));
#31290=DIRECTION('ref_axis',(-1.,0.,0.));
#31291=DIRECTION('',(-1.,0.,0.));
#31292=DIRECTION('',(0.,0.,1.));
#31293=DIRECTION('',(-1.,0.,0.));
#31294=DIRECTION('',(0.,0.,1.));
#31295=DIRECTION('center_axis',(1.,0.,0.));
#31296=DIRECTION('ref_axis',(0.,1.,0.));
#31297=DIRECTION('',(0.,1.,0.));
#31298=DIRECTION('',(0.,1.,0.));
#31299=DIRECTION('',(0.,0.,1.));
#31300=DIRECTION('center_axis',(0.,-1.,0.));
#31301=DIRECTION('ref_axis',(1.,0.,0.));
#31302=DIRECTION('',(1.,0.,0.));
#31303=DIRECTION('',(1.,0.,0.));
#31304=DIRECTION('',(0.,0.,1.));
#31305=DIRECTION('center_axis',(-1.,0.,0.));
#31306=DIRECTION('ref_axis',(0.,-1.,0.));
#31307=DIRECTION('',(0.,-1.,0.));
#31308=DIRECTION('',(0.,-1.,0.));
#31309=DIRECTION('center_axis',(0.,0.,1.));
#31310=DIRECTION('ref_axis',(1.,0.,0.));
#31311=DIRECTION('center_axis',(0.,0.,1.));
#31312=DIRECTION('ref_axis',(1.,0.,0.));
#49837=CARTESIAN_POINT('',(0.,0.,0.));
#49838=CARTESIAN_POINT('Origin',(14.,-1.5,5.1));
#49839=CARTESIAN_POINT('',(13.79,-1.5,5.1));
#49840=CARTESIAN_POINT('Origin',(14.,-1.5,5.1));
#49841=CARTESIAN_POINT('',(13.79,-1.5,6.));
#49842=CARTESIAN_POINT('',(13.79,-1.5,5.1));
#49843=CARTESIAN_POINT('Origin',(14.,-1.5,6.));
#49844=CARTESIAN_POINT('Origin',(14.,-1.5,5.1));
#49845=CARTESIAN_POINT('Origin',(12.5,1.5,5.1));
#49846=CARTESIAN_POINT('',(12.29,1.5,5.1));
#49847=CARTESIAN_POINT('Origin',(12.5,1.5,5.1));
#49848=CARTESIAN_POINT('',(12.29,1.5,6.));
#49849=CARTESIAN_POINT('',(12.29,1.5,5.1));
#49850=CARTESIAN_POINT('Origin',(12.5,1.5,6.));
#49851=CARTESIAN_POINT('Origin',(12.5,1.5,5.1));
#49852=CARTESIAN_POINT('Origin',(12.5,-1.5,5.1));
#49853=CARTESIAN_POINT('',(12.29,-1.5,5.1));
#49854=CARTESIAN_POINT('Origin',(12.5,-1.5,5.1));
#49855=CARTESIAN_POINT('',(12.29,-1.5,6.));
#49856=CARTESIAN_POINT('',(12.29,-1.5,5.1));
#49857=CARTESIAN_POINT('Origin',(12.5,-1.5,6.));
#49858=CARTESIAN_POINT('Origin',(12.5,-1.5,5.1));
#49859=CARTESIAN_POINT('Origin',(14.,1.5,5.1));
#49860=CARTESIAN_POINT('',(13.79,1.5,5.1));
#49861=CARTESIAN_POINT('Origin',(14.,1.5,5.1));
#49862=CARTESIAN_POINT('',(13.79,1.5,6.));
#49863=CARTESIAN_POINT('',(13.79,1.5,5.1));
#49864=CARTESIAN_POINT('Origin',(14.,1.5,6.));
#49865=CARTESIAN_POINT('Origin',(14.,1.5,5.1));
#49866=CARTESIAN_POINT('Origin',(12.9,-1.5,4.));
#49867=CARTESIAN_POINT('',(12.9,-1.5,4.165));
#49868=CARTESIAN_POINT('Origin',(12.9,-1.5,4.));
#49869=CARTESIAN_POINT('',(14.5,-1.5,4.165));
#49870=CARTESIAN_POINT('',(12.9,-1.5,4.165));
#49871=CARTESIAN_POINT('Origin',(14.5,-1.5,4.));
#49872=CARTESIAN_POINT('Origin',(12.9,-1.5,4.));
#49873=CARTESIAN_POINT('Origin',(12.9,1.5,4.));
#49874=CARTESIAN_POINT('',(12.9,1.5,4.165));
#49875=CARTESIAN_POINT('Origin',(12.9,1.5,4.));
#49876=CARTESIAN_POINT('',(14.5,1.5,4.165));
#49877=CARTESIAN_POINT('',(12.9,1.5,4.165));
#49878=CARTESIAN_POINT('Origin',(14.5,1.5,4.));
#49879=CARTESIAN_POINT('Origin',(12.9,1.5,4.));
#49880=CARTESIAN_POINT('Origin',(12.9,0.,5.5));
#49881=CARTESIAN_POINT('',(12.9,-2.02066721859313E-17,5.665));
#49882=CARTESIAN_POINT('Origin',(12.9,0.,5.5));
#49883=CARTESIAN_POINT('',(14.5,2.02066721859313E-17,5.665));
#49884=CARTESIAN_POINT('',(12.9,-2.02066721859313E-17,5.665));
#49885=CARTESIAN_POINT('Origin',(14.5,0.,5.5));
#49886=CARTESIAN_POINT('Origin',(12.9,0.,5.5));
#49887=CARTESIAN_POINT('Origin',(11.9,0.,4.));
#49888=CARTESIAN_POINT('',(12.,-1.35935794705356E-16,5.11));
#49889=CARTESIAN_POINT('Origin',(12.,0.,4.));
#49890=CARTESIAN_POINT('',(14.5,1.35935794705356E-16,5.11));
#49891=CARTESIAN_POINT('',(11.9,-1.35935794705356E-16,5.11));
#49892=CARTESIAN_POINT('Origin',(14.5,0.,4.));
#49893=CARTESIAN_POINT('Origin',(14.5,2.2,2.5));
#49894=CARTESIAN_POINT('',(14.5,2.2,2.5));
#49895=CARTESIAN_POINT('',(12.,2.2,2.5));
#49896=CARTESIAN_POINT('',(14.5,2.2,2.5));
#49897=CARTESIAN_POINT('',(12.,2.2,6.));
#49898=CARTESIAN_POINT('',(12.,2.2,2.5));
#49899=CARTESIAN_POINT('',(14.5,2.2,6.));
#49900=CARTESIAN_POINT('',(14.5,2.2,6.));
#49901=CARTESIAN_POINT('',(14.5,2.2,2.5));
#49902=CARTESIAN_POINT('Origin',(14.5,-2.2,2.5));
#49903=CARTESIAN_POINT('',(14.5,-2.2,2.5));
#49904=CARTESIAN_POINT('',(14.5,-2.2,2.5));
#49905=CARTESIAN_POINT('',(14.5,-2.2,6.));
#49906=CARTESIAN_POINT('',(14.5,-2.2,6.));
#49907=CARTESIAN_POINT('',(14.5,-2.2,2.5));
#49908=CARTESIAN_POINT('Origin',(12.,-2.2,2.5));
#49909=CARTESIAN_POINT('',(12.,-2.2,2.5));
#49910=CARTESIAN_POINT('',(12.,-2.2,2.5));
#49911=CARTESIAN_POINT('',(12.,-2.2,6.));
#49912=CARTESIAN_POINT('',(12.,-2.2,6.));
#49913=CARTESIAN_POINT('',(12.,-2.2,2.5));
#49914=CARTESIAN_POINT('Origin',(12.,2.2,2.5));
#49915=CARTESIAN_POINT('',(12.,2.2,2.5));
#49916=CARTESIAN_POINT('',(12.,2.2,6.));
#49917=CARTESIAN_POINT('Origin',(13.25,0.,6.));
#49918=CARTESIAN_POINT('Origin',(13.25,0.,2.5));
#62864=UNCERTAINTY_MEASURE_WITH_UNIT(LENGTH_MEASURE(0.001),#62985,
'DISTANCE_ACCURACY_VALUE',
'Maximum model space distance between geometric entities at asserted c
onnectivities');
#62885=UNCERTAINTY_MEASURE_WITH_UNIT(LENGTH_MEASURE(0.001),#62985,
'DISTANCE_ACCURACY_VALUE',
'Maximum model space distance between geometric entities at asserted c
onnectivities');
#62963=(
GEOMETRIC_REPRESENTATION_CONTEXT(3)
GLOBAL_UNCERTAINTY_ASSIGNED_CONTEXT((#62864))
GLOBAL_UNIT_ASSIGNED_CONTEXT((#62985,#62987,#62988))
REPRESENTATION_CONTEXT('','3D')
);
#62984=(
GEOMETRIC_REPRESENTATION_CONTEXT(3)
GLOBAL_UNCERTAINTY_ASSIGNED_CONTEXT((#62885))
GLOBAL_UNIT_ASSIGNED_CONTEXT((#62985,#62987,#62988))
REPRESENTATION_CONTEXT('','3D')
);
#62985=(
LENGTH_UNIT()
NAMED_UNIT(*)
SI_UNIT(.CENTI.,.METRE.)
);
#62987=(
NAMED_UNIT(*)
PLANE_ANGLE_UNIT()
SI_UNIT($,.RADIAN.)
);
#62988=(
NAMED_UNIT(*)
SI_UNIT($,.STERADIAN.)
SOLID_ANGLE_UNIT()
);
#63066=SHAPE_DEFINITION_REPRESENTATION(#63254,#63426);
#63254=PRODUCT_DEFINITION_SHAPE('',$,#63525);
#63426=SHAPE_REPRESENTATION('',(#25867),#62963);
#63447=PRODUCT_DEFINITION_CONTEXT('part definition',#63743,'design');
#63525=PRODUCT_DEFINITION('Y Stage - 07 Nut bracket',
'Y Stage - 07 Nut bracket',#63623,#63447);
#63623=PRODUCT_DEFINITION_FORMATION('',$,#63822);
#63743=APPLICATION_CONTEXT(
'Core Data for Automotive Mechanical Design Process');
#63744=PRODUCT_CONTEXT('part definition',#63743,'mechanical');
#63822=PRODUCT('Y Stage - 07 Nut bracket','Y Stage - 07 Nut bracket',
'Y Stage - 07 Nut bracket',(#63744));
#63913=COLOUR_RGB('Black',0.12,0.14,0.17);
#63914=FILL_AREA_STYLE_COLOUR('',#63913);
#63915=FILL_AREA_STYLE('',(#63914));
#63916=SURFACE_STYLE_FILL_AREA(#63915);
#63917=SURFACE_SIDE_STYLE('',(#63916));
#63918=SURFACE_STYLE_USAGE(.BOTH.,#63917);
#63919=PRESENTATION_STYLE_ASSIGNMENT((#63918));
ENDSEC;
END-ISO-10303-21;
